ISO-10303-21;
HEADER;
/* Generated by software containing ST-Developer
 * from STEP Tools, Inc. (www.steptools.com) 
 */

FILE_DESCRIPTION(
/* description */ ('Rigid flange shaft coupling assembly'),
/* implementation_level */ '2;1');

FILE_NAME(
/* name */ 'Hex Nut - M6.step',
/* time_stamp */ '2026-10-27T10:47:16-07:00',
/* author */ (''),
/* organization */ (''),
/* preprocessor_version */ 'ST-DEVELOPER v20.2',
/* originating_system */ 'Autodesk Translation Framework v15.17.0.0',
/* authorisation */ '');

FILE_SCHEMA (('AUTOMOTIVE_DESIGN { 1 0 10303 214 3 1 1 }'));
ENDSEC;

DATA;
#10=MECHANICAL_DESIGN_GEOMETRIC_PRESENTATION_REPRESENTATION('',(#425),#9141);
#11=(
BOUNDED_CURVE()
B_SPLINE_CURVE(2,(#8914,#8915,#8916),.UNSPECIFIED.,.F.,.F.)
B_SPLINE_CURVE_WITH_KNOTS((3,3),(0.144988513094728,0.791574906712449),
 .UNSPECIFIED.)
CURVE()
GEOMETRIC_REPRESENTATION_ITEM()
RATIONAL_B_SPLINE_CURVE((1.09282032302755,1.26188021535082,1.09282032302931))
REPRESENTATION_ITEM('')
);
#12=(
BOUNDED_CURVE()
B_SPLINE_CURVE(2,(#8918,#8919,#8920),.UNSPECIFIED.,.F.,.F.)
B_SPLINE_CURVE_WITH_KNOTS((3,3),(0.144988513094728,0.791574906712449),
 .UNSPECIFIED.)
CURVE()
GEOMETRIC_REPRESENTATION_ITEM()
RATIONAL_B_SPLINE_CURVE((1.09282032302755,1.26188021535082,1.09282032302931))
REPRESENTATION_ITEM('')
);
#13=(
BOUNDED_CURVE()
B_SPLINE_CURVE(2,(#8925,#8926,#8927),.UNSPECIFIED.,.F.,.F.)
B_SPLINE_CURVE_WITH_KNOTS((3,3),(0.144988513094728,0.791574906712449),
 .UNSPECIFIED.)
CURVE()
GEOMETRIC_REPRESENTATION_ITEM()
RATIONAL_B_SPLINE_CURVE((1.09282032302755,1.26188021535082,1.09282032302931))
REPRESENTATION_ITEM('')
);
#14=(
BOUNDED_CURVE()
B_SPLINE_CURVE(2,(#8929,#8930,#8931),.UNSPECIFIED.,.F.,.F.)
B_SPLINE_CURVE_WITH_KNOTS((3,3),(0.144988513094728,0.791574906712449),
 .UNSPECIFIED.)
CURVE()
GEOMETRIC_REPRESENTATION_ITEM()
RATIONAL_B_SPLINE_CURVE((1.09282032302755,1.26188021535082,1.09282032302931))
REPRESENTATION_ITEM('')
);
#15=(
BOUNDED_CURVE()
B_SPLINE_CURVE(2,(#8933,#8934,#8935),.UNSPECIFIED.,.F.,.F.)
B_SPLINE_CURVE_WITH_KNOTS((3,3),(0.144988513094728,0.791574906712449),
 .UNSPECIFIED.)
CURVE()
GEOMETRIC_REPRESENTATION_ITEM()
RATIONAL_B_SPLINE_CURVE((1.09282032302755,1.26188021535082,1.09282032302931))
REPRESENTATION_ITEM('')
);
#16=(
BOUNDED_CURVE()
B_SPLINE_CURVE(2,(#8936,#8937,#8938),.UNSPECIFIED.,.F.,.F.)
B_SPLINE_CURVE_WITH_KNOTS((3,3),(0.144988513094728,0.791574906712449),
 .UNSPECIFIED.)
CURVE()
GEOMETRIC_REPRESENTATION_ITEM()
RATIONAL_B_SPLINE_CURVE((1.09282032302755,1.26188021535082,1.09282032302931))
REPRESENTATION_ITEM('')
);
#17=(
BOUNDED_CURVE()
B_SPLINE_CURVE(2,(#8945,#8946,#8947),.UNSPECIFIED.,.F.,.F.)
B_SPLINE_CURVE_WITH_KNOTS((3,3),(0.144988513094728,0.791574906712449),
 .UNSPECIFIED.)
CURVE()
GEOMETRIC_REPRESENTATION_ITEM()
RATIONAL_B_SPLINE_CURVE((1.09282032302755,1.26188021535082,1.09282032302931))
REPRESENTATION_ITEM('')
);
#18=(
BOUNDED_CURVE()
B_SPLINE_CURVE(2,(#8949,#8950,#8951),.UNSPECIFIED.,.F.,.F.)
B_SPLINE_CURVE_WITH_KNOTS((3,3),(0.144988513094727,0.791574906712449),
 .UNSPECIFIED.)
CURVE()
GEOMETRIC_REPRESENTATION_ITEM()
RATIONAL_B_SPLINE_CURVE((1.09282032302755,1.26188021535082,1.09282032302931))
REPRESENTATION_ITEM('')
);
#19=(
BOUNDED_CURVE()
B_SPLINE_CURVE(2,(#8953,#8954,#8955),.UNSPECIFIED.,.F.,.F.)
B_SPLINE_CURVE_WITH_KNOTS((3,3),(0.144988513094728,0.791574906712449),
 .UNSPECIFIED.)
CURVE()
GEOMETRIC_REPRESENTATION_ITEM()
RATIONAL_B_SPLINE_CURVE((1.09282032302755,1.26188021535082,1.09282032302931))
REPRESENTATION_ITEM('')
);
#20=(
BOUNDED_CURVE()
B_SPLINE_CURVE(2,(#8957,#8958,#8959),.UNSPECIFIED.,.F.,.F.)
B_SPLINE_CURVE_WITH_KNOTS((3,3),(0.144988513094728,0.791574906712449),
 .UNSPECIFIED.)
CURVE()
GEOMETRIC_REPRESENTATION_ITEM()
RATIONAL_B_SPLINE_CURVE((1.09282032302755,1.26188021535082,1.09282032302931))
REPRESENTATION_ITEM('')
);
#21=(
BOUNDED_CURVE()
B_SPLINE_CURVE(2,(#8961,#8962,#8963),.UNSPECIFIED.,.F.,.F.)
B_SPLINE_CURVE_WITH_KNOTS((3,3),(0.144988513094728,0.791574906712449),
 .UNSPECIFIED.)
CURVE()
GEOMETRIC_REPRESENTATION_ITEM()
RATIONAL_B_SPLINE_CURVE((1.09282032302755,1.26188021535082,1.09282032302931))
REPRESENTATION_ITEM('')
);
#22=(
BOUNDED_CURVE()
B_SPLINE_CURVE(2,(#8964,#8965,#8966),.UNSPECIFIED.,.F.,.F.)
B_SPLINE_CURVE_WITH_KNOTS((3,3),(0.144988513094727,0.791574906712449),
 .UNSPECIFIED.)
CURVE()
GEOMETRIC_REPRESENTATION_ITEM()
RATIONAL_B_SPLINE_CURVE((1.09282032302755,1.26188021535082,1.09282032302931))
REPRESENTATION_ITEM('')
);
#34=CONICAL_SURFACE('',#5575,0.576175134594813,1.0471975511966);
#35=CONICAL_SURFACE('',#5577,0.576175134594813,1.0471975511966);
#368=SHAPE_REPRESENTATION_RELATIONSHIP('SRR','None',#9304,#396);
#396=ADVANCED_BREP_SHAPE_REPRESENTATION('',(#451),#9139);
#425=STYLED_ITEM('',(#9507),#451);
#451=MANIFOLD_SOLID_BREP('Body1',#4782);
#567=FACE_BOUND('',#1389,.T.);
#568=FACE_BOUND('',#1391,.T.);
#727=PLANE('',#5579);
#728=PLANE('',#5580);
#729=PLANE('',#5581);
#730=PLANE('',#5585);
#731=PLANE('',#5586);
#732=PLANE('',#5587);
#733=PLANE('',#5588);
#734=PLANE('',#5589);
#993=FACE_OUTER_BOUND('',#1379,.T.);
#994=FACE_OUTER_BOUND('',#1380,.T.);
#995=FACE_OUTER_BOUND('',#1381,.T.);
#996=FACE_OUTER_BOUND('',#1382,.T.);
#997=FACE_OUTER_BOUND('',#1383,.T.);
#998=FACE_OUTER_BOUND('',#1384,.T.);
#999=FACE_OUTER_BOUND('',#1385,.T.);
#1000=FACE_OUTER_BOUND('',#1386,.T.);
#1001=FACE_OUTER_BOUND('',#1387,.T.);
#1002=FACE_OUTER_BOUND('',#1388,.T.);
#1003=FACE_OUTER_BOUND('',#1390,.T.);
#1379=EDGE_LOOP('',(#4299,#4300,#4301,#4302,#4303,#4304,#4305,#4306,#4307));
#1380=EDGE_LOOP('',(#4308,#4309,#4310,#4311,#4312,#4313,#4314,#4315,#4316));
#1381=EDGE_LOOP('',(#4317,#4318,#4319,#4320));
#1382=EDGE_LOOP('',(#4321,#4322,#4323,#4324));
#1383=EDGE_LOOP('',(#4325,#4326,#4327,#4328));
#1384=EDGE_LOOP('',(#4329,#4330,#4331,#4332));
#1385=EDGE_LOOP('',(#4333,#4334,#4335,#4336));
#1386=EDGE_LOOP('',(#4337,#4338,#4339,#4340));
#1387=EDGE_LOOP('',(#4341,#4342,#4343,#4344));
#1388=EDGE_LOOP('',(#4345));
#1389=EDGE_LOOP('',(#4346));
#1390=EDGE_LOOP('',(#4347));
#1391=EDGE_LOOP('',(#4348));
#1720=LINE('',#8922,#2065);
#1721=LINE('',#8943,#2066);
#1722=LINE('',#8968,#2067);
#1723=LINE('',#8969,#2068);
#1724=LINE('',#8971,#2069);
#1725=LINE('',#8973,#2070);
#1726=LINE('',#8978,#2071);
#1727=LINE('',#8981,#2072);
#1728=LINE('',#8983,#2073);
#2065=VECTOR('',#6923,0.576175134594813);
#2066=VECTOR('',#6930,0.576175134594813);
#2067=VECTOR('',#6933,1.);
#2068=VECTOR('',#6934,1.);
#2069=VECTOR('',#6937,1.);
#2070=VECTOR('',#6940,1.);
#2071=VECTOR('',#6945,0.3);
#2072=VECTOR('',#6950,1.);
#2073=VECTOR('',#6953,1.);
#2268=CIRCLE('',#5576,0.475);
#2269=CIRCLE('',#5578,0.475);
#2270=CIRCLE('',#5583,0.25175);
#2271=CIRCLE('',#5584,0.25175);
#2633=VERTEX_POINT('',#8912);
#2634=VERTEX_POINT('',#8913);
#2635=VERTEX_POINT('',#8917);
#2636=VERTEX_POINT('',#8921);
#2637=VERTEX_POINT('',#8924);
#2638=VERTEX_POINT('',#8928);
#2639=VERTEX_POINT('',#8932);
#2640=VERTEX_POINT('',#8940);
#2641=VERTEX_POINT('',#8942);
#2642=VERTEX_POINT('',#8944);
#2643=VERTEX_POINT('',#8948);
#2644=VERTEX_POINT('',#8952);
#2645=VERTEX_POINT('',#8956);
#2646=VERTEX_POINT('',#8960);
#2647=VERTEX_POINT('',#8975);
#2648=VERTEX_POINT('',#8977);
#3193=EDGE_CURVE('',#2633,#2634,#11,.T.);
#3194=EDGE_CURVE('',#2635,#2633,#12,.T.);
#3195=EDGE_CURVE('',#2635,#2636,#1720,.T.);
#3196=EDGE_CURVE('',#2636,#2636,#2268,.T.);
#3197=EDGE_CURVE('',#2637,#2635,#13,.T.);
#3198=EDGE_CURVE('',#2638,#2637,#14,.T.);
#3199=EDGE_CURVE('',#2639,#2638,#15,.T.);
#3200=EDGE_CURVE('',#2634,#2639,#16,.T.);
#3201=EDGE_CURVE('',#2640,#2640,#2269,.T.);
#3202=EDGE_CURVE('',#2640,#2641,#1721,.T.);
#3203=EDGE_CURVE('',#2642,#2641,#17,.T.);
#3204=EDGE_CURVE('',#2643,#2642,#18,.T.);
#3205=EDGE_CURVE('',#2644,#2643,#19,.T.);
#3206=EDGE_CURVE('',#2645,#2644,#20,.T.);
#3207=EDGE_CURVE('',#2646,#2645,#21,.T.);
#3208=EDGE_CURVE('',#2641,#2646,#22,.T.);
#3209=EDGE_CURVE('',#2637,#2646,#1722,.T.);
#3210=EDGE_CURVE('',#2638,#2645,#1723,.T.);
#3211=EDGE_CURVE('',#2635,#2641,#1724,.T.);
#3212=EDGE_CURVE('',#2633,#2642,#1725,.T.);
#3213=EDGE_CURVE('',#2647,#2647,#2270,.F.);
#3214=EDGE_CURVE('',#2647,#2648,#1726,.T.);
#3215=EDGE_CURVE('',#2648,#2648,#2271,.F.);
#3216=EDGE_CURVE('',#2634,#2643,#1727,.T.);
#3217=EDGE_CURVE('',#2639,#2644,#1728,.T.);
#4299=ORIENTED_EDGE('',*,*,#3193,.F.);
#4300=ORIENTED_EDGE('',*,*,#3194,.F.);
#4301=ORIENTED_EDGE('',*,*,#3195,.T.);
#4302=ORIENTED_EDGE('',*,*,#3196,.F.);
#4303=ORIENTED_EDGE('',*,*,#3195,.F.);
#4304=ORIENTED_EDGE('',*,*,#3197,.F.);
#4305=ORIENTED_EDGE('',*,*,#3198,.F.);
#4306=ORIENTED_EDGE('',*,*,#3199,.F.);
#4307=ORIENTED_EDGE('',*,*,#3200,.F.);
#4308=ORIENTED_EDGE('',*,*,#3201,.F.);
#4309=ORIENTED_EDGE('',*,*,#3202,.T.);
#4310=ORIENTED_EDGE('',*,*,#3203,.F.);
#4311=ORIENTED_EDGE('',*,*,#3204,.F.);
#4312=ORIENTED_EDGE('',*,*,#3205,.F.);
#4313=ORIENTED_EDGE('',*,*,#3206,.F.);
#4314=ORIENTED_EDGE('',*,*,#3207,.F.);
#4315=ORIENTED_EDGE('',*,*,#3208,.F.);
#4316=ORIENTED_EDGE('',*,*,#3202,.F.);
#4317=ORIENTED_EDGE('',*,*,#3198,.T.);
#4318=ORIENTED_EDGE('',*,*,#3209,.T.);
#4319=ORIENTED_EDGE('',*,*,#3207,.T.);
#4320=ORIENTED_EDGE('',*,*,#3210,.F.);
#4321=ORIENTED_EDGE('',*,*,#3197,.T.);
#4322=ORIENTED_EDGE('',*,*,#3211,.T.);
#4323=ORIENTED_EDGE('',*,*,#3208,.T.);
#4324=ORIENTED_EDGE('',*,*,#3209,.F.);
#4325=ORIENTED_EDGE('',*,*,#3194,.T.);
#4326=ORIENTED_EDGE('',*,*,#3212,.T.);
#4327=ORIENTED_EDGE('',*,*,#3203,.T.);
#4328=ORIENTED_EDGE('',*,*,#3211,.F.);
#4329=ORIENTED_EDGE('',*,*,#3213,.F.);
#4330=ORIENTED_EDGE('',*,*,#3214,.T.);
#4331=ORIENTED_EDGE('',*,*,#3215,.T.);
#4332=ORIENTED_EDGE('',*,*,#3214,.F.);
#4333=ORIENTED_EDGE('',*,*,#3193,.T.);
#4334=ORIENTED_EDGE('',*,*,#3216,.T.);
#4335=ORIENTED_EDGE('',*,*,#3204,.T.);
#4336=ORIENTED_EDGE('',*,*,#3212,.F.);
#4337=ORIENTED_EDGE('',*,*,#3199,.T.);
#4338=ORIENTED_EDGE('',*,*,#3210,.T.);
#4339=ORIENTED_EDGE('',*,*,#3206,.T.);
#4340=ORIENTED_EDGE('',*,*,#3217,.F.);
#4341=ORIENTED_EDGE('',*,*,#3200,.T.);
#4342=ORIENTED_EDGE('',*,*,#3217,.T.);
#4343=ORIENTED_EDGE('',*,*,#3205,.T.);
#4344=ORIENTED_EDGE('',*,*,#3216,.F.);
#4345=ORIENTED_EDGE('',*,*,#3201,.T.);
#4346=ORIENTED_EDGE('',*,*,#3213,.T.);
#4347=ORIENTED_EDGE('',*,*,#3196,.T.);
#4348=ORIENTED_EDGE('',*,*,#3215,.F.);
#4478=CYLINDRICAL_SURFACE('',#5582,0.25175);
#4729=ADVANCED_FACE('',(#993),#34,.T.);
#4730=ADVANCED_FACE('',(#994),#35,.T.);
#4731=ADVANCED_FACE('',(#995),#727,.T.);
#4732=ADVANCED_FACE('',(#996),#728,.T.);
#4733=ADVANCED_FACE('',(#997),#729,.T.);
#4734=ADVANCED_FACE('',(#998),#4478,.F.);
#4735=ADVANCED_FACE('',(#999),#730,.T.);
#4736=ADVANCED_FACE('',(#1000),#731,.T.);
#4737=ADVANCED_FACE('',(#1001),#732,.T.);
#4738=ADVANCED_FACE('',(#1002,#567),#733,.T.);
#4739=ADVANCED_FACE('',(#1003,#568),#734,.F.);
#4782=CLOSED_SHELL('',(#4729,#4730,#4731,#4732,#4733,#4734,#4735,#4736,
#4737,#4738,#4739));
#5574=AXIS2_PLACEMENT_3D('',#8910,#6919,#6920);
#5575=AXIS2_PLACEMENT_3D('',#8911,#6921,#6922);
#5576=AXIS2_PLACEMENT_3D('',#8923,#6924,#6925);
#5577=AXIS2_PLACEMENT_3D('',#8939,#6926,#6927);
#5578=AXIS2_PLACEMENT_3D('',#8941,#6928,#6929);
#5579=AXIS2_PLACEMENT_3D('',#8967,#6931,#6932);
#5580=AXIS2_PLACEMENT_3D('',#8970,#6935,#6936);
#5581=AXIS2_PLACEMENT_3D('',#8972,#6938,#6939);
#5582=AXIS2_PLACEMENT_3D('',#8974,#6941,#6942);
#5583=AXIS2_PLACEMENT_3D('',#8976,#6943,#6944);
#5584=AXIS2_PLACEMENT_3D('',#8979,#6946,#6947);
#5585=AXIS2_PLACEMENT_3D('',#8980,#6948,#6949);
#5586=AXIS2_PLACEMENT_3D('',#8982,#6951,#6952);
#5587=AXIS2_PLACEMENT_3D('',#8984,#6954,#6955);
#5588=AXIS2_PLACEMENT_3D('',#8985,#6956,#6957);
#5589=AXIS2_PLACEMENT_3D('',#8986,#6958,#6959);
#6919=DIRECTION('axis',(0.,0.,1.));
#6920=DIRECTION('refdir',(1.,0.,0.));
#6921=DIRECTION('center_axis',(0.,1.,0.));
#6922=DIRECTION('ref_axis',(1.,0.,0.));
#6923=DIRECTION('',(0.866025403784439,-0.5,1.06057523872491E-16));
#6924=DIRECTION('center_axis',(0.,-1.,0.));
#6925=DIRECTION('ref_axis',(1.,0.,0.));
#6926=DIRECTION('center_axis',(0.,-1.,0.));
#6927=DIRECTION('ref_axis',(1.,0.,0.));
#6928=DIRECTION('center_axis',(0.,1.,0.));
#6929=DIRECTION('ref_axis',(1.,0.,0.));
#6930=DIRECTION('',(-0.866025403784439,-0.5,-1.06057523872491E-16));
#6931=DIRECTION('center_axis',(1.92296268638356E-16,0.,-1.));
#6932=DIRECTION('ref_axis',(-1.,0.,-1.92296268638356E-16));
#6933=DIRECTION('',(0.,1.,0.));
#6934=DIRECTION('',(0.,1.,0.));
#6935=DIRECTION('center_axis',(-0.866025403784439,0.,-0.5));
#6936=DIRECTION('ref_axis',(-0.5,0.,0.866025403784439));
#6937=DIRECTION('',(0.,1.,0.));
#6938=DIRECTION('center_axis',(-0.866025403784439,0.,0.5));
#6939=DIRECTION('ref_axis',(0.5,0.,0.866025403784439));
#6940=DIRECTION('',(0.,1.,0.));
#6941=DIRECTION('center_axis',(0.,1.,0.));
#6942=DIRECTION('ref_axis',(1.,0.,0.));
#6943=DIRECTION('center_axis',(0.,1.,0.));
#6944=DIRECTION('ref_axis',(1.,0.,0.));
#6945=DIRECTION('',(0.,-1.,0.));
#6946=DIRECTION('center_axis',(0.,1.,0.));
#6947=DIRECTION('ref_axis',(1.,0.,0.));
#6948=DIRECTION('center_axis',(-1.92296268638356E-16,0.,1.));
#6949=DIRECTION('ref_axis',(1.,0.,1.92296268638356E-16));
#6950=DIRECTION('',(0.,1.,0.));
#6951=DIRECTION('center_axis',(0.866025403784439,0.,-0.5));
#6952=DIRECTION('ref_axis',(-0.5,0.,-0.866025403784439));
#6953=DIRECTION('',(0.,1.,0.));
#6954=DIRECTION('center_axis',(0.866025403784439,0.,0.5));
#6955=DIRECTION('ref_axis',(0.5,0.,-0.866025403784439));
#6956=DIRECTION('center_axis',(0.,1.,0.));
#6957=DIRECTION('ref_axis',(1.,0.,0.));
#6958=DIRECTION('center_axis',(0.,1.,0.));
#6959=DIRECTION('ref_axis',(1.,0.,0.));
#8910=CARTESIAN_POINT('',(0.,0.,0.));
#8911=CARTESIAN_POINT('Origin',(0.,0.0584134911936118,0.));
#8912=CARTESIAN_POINT('',(-0.288675134594813,0.0590919554682611,0.5));
#8913=CARTESIAN_POINT('',(0.288675134594813,0.0590919554682611,0.5));
#8914=CARTESIAN_POINT('Ctrl Pts',(-0.288675134594813,0.0590919554682611,
0.5));
#8915=CARTESIAN_POINT('Ctrl Pts',(2.1664336991023E-12,-0.0242413778636964,
0.5));
#8916=CARTESIAN_POINT('Ctrl Pts',(0.288675134594813,0.0590919554682611,
0.5));
#8917=CARTESIAN_POINT('',(-0.577350269189626,0.0590919554682611,-7.07050159149938E-17));
#8918=CARTESIAN_POINT('Ctrl Pts',(-0.577350269189626,0.0590919554682611,
-7.07050159149938E-17));
#8919=CARTESIAN_POINT('Ctrl Pts',(-0.433012701891136,-0.0242413778636963,
0.250000000001876));
#8920=CARTESIAN_POINT('Ctrl Pts',(-0.288675134594813,0.0590919554682611,
0.5));
#8921=CARTESIAN_POINT('',(-0.475,-4.16333634234434E-17,-5.81707229594993E-17));
#8922=CARTESIAN_POINT('',(-0.576175134594813,0.0584134911936118,-7.05611034329833E-17));
#8923=CARTESIAN_POINT('Origin',(0.,0.,0.));
#8924=CARTESIAN_POINT('',(-0.288675134594813,0.0590919554682611,-0.5));
#8925=CARTESIAN_POINT('Ctrl Pts',(-0.288675134594813,0.0590919554682611,
-0.5));
#8926=CARTESIAN_POINT('Ctrl Pts',(-0.433012701893303,-0.0242413778636963,
-0.249999999998124));
#8927=CARTESIAN_POINT('Ctrl Pts',(-0.577350269189626,0.0590919554682611,
-7.07050159149938E-17));
#8928=CARTESIAN_POINT('',(0.288675134594813,0.0590919554682611,-0.5));
#8929=CARTESIAN_POINT('Ctrl Pts',(0.288675134594813,0.0590919554682611,
-0.5));
#8930=CARTESIAN_POINT('Ctrl Pts',(-2.16648921025353E-12,-0.0242413778636962,
-0.5));
#8931=CARTESIAN_POINT('Ctrl Pts',(-0.288675134594813,0.0590919554682611,
-0.5));
#8932=CARTESIAN_POINT('',(0.577350269189626,0.0590919554682611,0.));
#8933=CARTESIAN_POINT('Ctrl Pts',(0.577350269189626,0.0590919554682611,
0.));
#8934=CARTESIAN_POINT('Ctrl Pts',(0.433012701891136,-0.0242413778636963,
-0.250000000001876));
#8935=CARTESIAN_POINT('Ctrl Pts',(0.288675134594813,0.0590919554682611,
-0.5));
#8936=CARTESIAN_POINT('Ctrl Pts',(0.288675134594813,0.0590919554682611,
0.5));
#8937=CARTESIAN_POINT('Ctrl Pts',(0.433012701893303,-0.0242413778636962,
0.249999999998124));
#8938=CARTESIAN_POINT('Ctrl Pts',(0.577350269189626,0.0590919554682611,
0.));
#8939=CARTESIAN_POINT('Origin',(0.,0.461586508806388,0.));
#8940=CARTESIAN_POINT('',(-0.475,0.52,-5.81707229594993E-17));
#8941=CARTESIAN_POINT('Origin',(0.,0.52,0.));
#8942=CARTESIAN_POINT('',(-0.577350269189626,0.460908044531739,-7.07050159149938E-17));
#8943=CARTESIAN_POINT('',(-0.576175134594813,0.461586508806388,-7.05611034329833E-17));
#8944=CARTESIAN_POINT('',(-0.288675134594813,0.460908044531739,0.5));
#8945=CARTESIAN_POINT('Ctrl Pts',(-0.288675134594813,0.460908044531739,
0.5));
#8946=CARTESIAN_POINT('Ctrl Pts',(-0.433012701893303,0.544241377863696,
0.249999999998124));
#8947=CARTESIAN_POINT('Ctrl Pts',(-0.577350269189626,0.460908044531739,
-7.07050159149938E-17));
#8948=CARTESIAN_POINT('',(0.288675134594813,0.460908044531739,0.5));
#8949=CARTESIAN_POINT('Ctrl Pts',(0.288675134594813,0.460908044531739,0.5));
#8950=CARTESIAN_POINT('Ctrl Pts',(-2.16676676600969E-12,0.544241377863697,
0.5));
#8951=CARTESIAN_POINT('Ctrl Pts',(-0.288675134594813,0.460908044531739,
0.5));
#8952=CARTESIAN_POINT('',(0.577350269189626,0.460908044531739,0.));
#8953=CARTESIAN_POINT('Ctrl Pts',(0.577350269189626,0.460908044531739,0.));
#8954=CARTESIAN_POINT('Ctrl Pts',(0.433012701891136,0.544241377863696,0.250000000001876));
#8955=CARTESIAN_POINT('Ctrl Pts',(0.288675134594813,0.460908044531739,0.5));
#8956=CARTESIAN_POINT('',(0.288675134594813,0.460908044531739,-0.5));
#8957=CARTESIAN_POINT('Ctrl Pts',(0.288675134594813,0.460908044531739,-0.5));
#8958=CARTESIAN_POINT('Ctrl Pts',(0.433012701893302,0.544241377863696,-0.249999999998124));
#8959=CARTESIAN_POINT('Ctrl Pts',(0.577350269189626,0.460908044531739,0.));
#8960=CARTESIAN_POINT('',(-0.288675134594813,0.460908044531739,-0.5));
#8961=CARTESIAN_POINT('Ctrl Pts',(-0.288675134594813,0.460908044531739,
-0.5));
#8962=CARTESIAN_POINT('Ctrl Pts',(2.16660023255599E-12,0.544241377863697,
-0.5));
#8963=CARTESIAN_POINT('Ctrl Pts',(0.288675134594813,0.460908044531739,-0.5));
#8964=CARTESIAN_POINT('Ctrl Pts',(-0.577350269189626,0.460908044531739,
-7.07050159149938E-17));
#8965=CARTESIAN_POINT('Ctrl Pts',(-0.433012701891136,0.544241377863696,
-0.250000000001876));
#8966=CARTESIAN_POINT('Ctrl Pts',(-0.288675134594813,0.460908044531739,
-0.5));
#8967=CARTESIAN_POINT('Origin',(0.288675134594813,0.,-0.5));
#8968=CARTESIAN_POINT('',(-0.288675134594813,0.,-0.5));
#8969=CARTESIAN_POINT('',(0.288675134594813,0.,-0.5));
#8970=CARTESIAN_POINT('Origin',(-0.288675134594813,0.,-0.5));
#8971=CARTESIAN_POINT('',(-0.577350269189626,0.,-7.07050159149938E-17));
#8972=CARTESIAN_POINT('Origin',(-0.577350269189626,0.,-7.07050159149938E-17));
#8973=CARTESIAN_POINT('',(-0.288675134594813,0.,0.5));
#8974=CARTESIAN_POINT('Origin',(0.,0.,0.));
#8975=CARTESIAN_POINT('',(-0.25175,0.52,3.08304831685346E-17));
#8976=CARTESIAN_POINT('Origin',(0.,0.52,0.));
#8977=CARTESIAN_POINT('',(-0.25175,0.,3.08304831685346E-17));
#8978=CARTESIAN_POINT('',(-0.25175,0.,3.08304831685346E-17));
#8979=CARTESIAN_POINT('Origin',(0.,0.,0.));
#8980=CARTESIAN_POINT('Origin',(-0.288675134594813,0.,0.5));
#8981=CARTESIAN_POINT('',(0.288675134594813,0.,0.5));
#8982=CARTESIAN_POINT('Origin',(0.577350269189626,0.,0.));
#8983=CARTESIAN_POINT('',(0.577350269189626,0.,0.));
#8984=CARTESIAN_POINT('Origin',(0.288675134594813,0.,0.5));
#8985=CARTESIAN_POINT('Origin',(0.,0.52,0.));
#8986=CARTESIAN_POINT('Origin',(0.,0.,0.));
#9106=UNCERTAINTY_MEASURE_WITH_UNIT(LENGTH_MEASURE(0.001),#9142,
'DISTANCE_ACCURACY_VALUE',
'Maximum model space distance between geometric entities at asserted c
onnectivities');
#9108=UNCERTAINTY_MEASURE_WITH_UNIT(LENGTH_MEASURE(0.001),#9142,
'DISTANCE_ACCURACY_VALUE',
'Maximum model space distance between geometric entities at asserted c
onnectivities');
#9139=(
GEOMETRIC_REPRESENTATION_CONTEXT(3)
GLOBAL_UNCERTAINTY_ASSIGNED_CONTEXT((#9106))
GLOBAL_UNIT_ASSIGNED_CONTEXT((#9142,#9144,#9145))
REPRESENTATION_CONTEXT('','3D')
);
#9141=(
GEOMETRIC_REPRESENTATION_CONTEXT(3)
GLOBAL_UNCERTAINTY_ASSIGNED_CONTEXT((#9108))
GLOBAL_UNIT_ASSIGNED_CONTEXT((#9142,#9144,#9145))
REPRESENTATION_CONTEXT('','3D')
);
#9142=(
LENGTH_UNIT()
NAMED_UNIT(*)
SI_UNIT(.CENTI.,.METRE.)
);
#9144=(
NAMED_UNIT(*)
PLANE_ANGLE_UNIT()
SI_UNIT($,.RADIAN.)
);
#9145=(
NAMED_UNIT(*)
SI_UNIT($,.STERADIAN.)
SOLID_ANGLE_UNIT()
);
#9176=SHAPE_DEFINITION_REPRESENTATION(#9237,#9304);
#9237=PRODUCT_DEFINITION_SHAPE('',$,#9337);
#9304=SHAPE_REPRESENTATION('',(#5574),#9139);
#9306=PRODUCT_DEFINITION_CONTEXT('part definition',#9404,'design');
#9337=PRODUCT_DEFINITION('Hex Nut - M6','Hex Nut - M6',#9369,#9306);
#9369=PRODUCT_DEFINITION_FORMATION('',$,#9436);
#9404=APPLICATION_CONTEXT(
'Core Data for Automotive Mechanical Design Process');
#9405=PRODUCT_CONTEXT('part definition',#9404,'mechanical');
#9436=PRODUCT('Hex Nut - M6','Hex Nut - M6','Hex Nut - M6',(#9405));
#9501=COLOUR_RGB('Black',0.12,0.14,0.17);
#9502=FILL_AREA_STYLE_COLOUR('',#9501);
#9503=FILL_AREA_STYLE('',(#9502));
#9504=SURFACE_STYLE_FILL_AREA(#9503);
#9505=SURFACE_SIDE_STYLE('',(#9504));
#9506=SURFACE_STYLE_USAGE(.BOTH.,#9505);
#9507=PRESENTATION_STYLE_ASSIGNMENT((#9506));
ENDSEC;
END-ISO-10303-21;
